ISO-10303-21;
HEADER;
FILE_DESCRIPTION (('STEP AP214'),
    '1' );
FILE_NAME ('socket head cap screw_am_B18.3.1M - 8 x 1.25 x 25 Hex SHCS -- 25NHX.step',
    '2026-10-24T15:53:57',
    ( '' ),
    ( '' ),
    'SwSTEP 2.0',
    'SolidWorks 2025',
    '' );
FILE_SCHEMA (( 'AUTOMOTIVE_DESIGN' ));
ENDSEC;

DATA;
#7=EDGE_LOOP ( 'NONE', ( #379, #934, #6709, #4880 ) ) ;
#22=CIRCLE ( 'NONE', #1145, 3.047499999999999876 ) ;
#25=ORIENTED_EDGE ( 'NONE', *, *, #2156, .F. ) ;
#31=DIRECTION ( 'NONE',  ( 1.000000000000000000, -3.549874073494553124E-30, -3.778304382545602261E-59 ) ) ;
#90=ORIENTED_EDGE ( 'NONE', *, *, #5306, .F. ) ;
#108=EDGE_CURVE ( 'NONE', #7841, #5835, #6535, .T. ) ;
#112=CARTESIAN_POINT ( 'NONE',  ( 2.651878572103346281E-45, 7.470345474798193622E-16, 5.700000000000001954 ) ) ;
#114=VECTOR ( 'NONE', #3316, 1000.000000000000000 ) ;
#116=CARTESIAN_POINT ( 'NONE',  ( 33.00000000000055422, -1.431146867680869324E-14, 3.309500000006883269 ) ) ;
#122=LINE ( 'NONE', #2790, #5242 ) ;
#124=ORIENTED_EDGE ( 'NONE', *, *, #2890, .F. ) ;
#138=DIRECTION ( 'NONE',  ( 0.000000000000000000, -1.865174681370262041E-14, -1.000000000000000000 ) ) ;
#144=EDGE_CURVE ( 'NONE', #3620, #2938, #3568, .T. ) ;
#149=EDGE_LOOP ( 'NONE', ( #8051, #8502, #8444, #3963, #8407 ) ) ;
#153=EDGE_CURVE ( 'NONE', #8158, #6208, #162, .T. ) ;
#162=CIRCLE ( 'NONE', #5164, 5.700000000000001954 ) ;
#166=( NAMED_UNIT ( * ) SI_UNIT ( $, .STERADIAN. ) SOLID_ANGLE_UNIT ( ) );
#171=VECTOR ( 'NONE', #3121, 999.9999999999998863 ) ;
#173=VERTEX_POINT ( 'NONE', #4952 ) ;
#177=EDGE_CURVE ( 'NONE', #5857, #5352, #6924, .T. ) ;
#204=DIRECTION ( 'NONE',  ( 1.000000000000000000, -3.549874073494553124E-30, 0.000000000000000000 ) ) ;
#232=VERTEX_POINT ( 'NONE', #290 ) ;
#236=EDGE_LOOP ( 'NONE', ( #4101, #6935, #4324 ) ) ;
#240=ORIENTED_EDGE ( 'NONE', *, *, #8498, .T. ) ;
#244=PLANE ( 'NONE',  #5375 ) ;
#249=CARTESIAN_POINT ( 'NONE',  ( 5.551115123125782702E-14, 3.518949890710790118, 2.220446049250313081E-13 ) ) ;
#250=ORIENTED_EDGE ( 'NONE', *, *, #1425, .T. ) ;
#251=DIRECTION ( 'NONE',  ( 0.000000000000000000, -1.213383262747659708E-29, 1.000000000000000000 ) ) ;
#255=ORIENTED_EDGE ( 'NONE', *, *, #2015, .T. ) ;
#259=CIRCLE ( 'NONE', #4435, 3.047499999999999876 ) ;
#273=CIRCLE ( 'NONE', #8348, 6.500000000000000888 ) ;
#276=DIRECTION ( 'NONE',  ( 3.549874073494553124E-30, 1.000000000000000000, -1.224646799147246711E-16 ) ) ;
#290=CARTESIAN_POINT ( 'NONE',  ( 4.000000000000003553, 1.759474945355374409, 3.047499999999869758 ) ) ;
#298=( LENGTH_UNIT ( ) NAMED_UNIT ( * ) SI_UNIT ( .MILLI., .METRE. ) );
#301=CYLINDRICAL_SURFACE ( 'NONE', #1407, 6.500000000000001776 ) ;
#321=ORIENTED_EDGE ( 'NONE', *, *, #108, .F. ) ;
#325=EDGE_LOOP ( 'NONE', ( #1288, #5702, #5068, #5725 ) ) ;
#334=CARTESIAN_POINT ( 'NONE',  ( -31.74999999999994316, -6.918267515436165433E-29, 6.500000000000001776 ) ) ;
#379=ORIENTED_EDGE ( 'NONE', *, *, #5089, .T. ) ;
#391=EDGE_CURVE ( 'NONE', #8158, #7966, #6399, .T. ) ;
#403=DIRECTION ( 'NONE',  ( 0.000000000000000000, -1.064348848528640545E-29, 1.000000000000000000 ) ) ;
#404=LINE ( 'NONE', #449, #7910 ) ;
#432=CIRCLE ( 'NONE', #8482, 4.000000000000060396 ) ;
#440=CARTESIAN_POINT ( 'NONE',  ( 8.000000000000007105, 7.960204194471028619E-16, -6.499999999999334754 ) ) ;
#445=EDGE_CURVE ( 'NONE', #1642, #1712, #1258, .T. ) ;
#449=CARTESIAN_POINT ( 'NONE',  ( 33.00000000000055422, -1.431146867680869324E-14, 3.309500000006883269 ) ) ;
#466=DIRECTION ( 'NONE',  ( 0.000000000000000000, 0.4999999999999986677, -0.8660254037844393737 ) ) ;
#471=CARTESIAN_POINT ( 'NONE',  ( 2.477984895244330595E-45, 6.980486755139308644E-16, 5.700000000000001954 ) ) ;
#483=DIRECTION ( 'NONE',  ( 0.000000000000000000, -1.064348848528640545E-29, 1.000000000000000000 ) ) ;
#498=EDGE_CURVE ( 'NONE', #173, #232, #3606, .T. ) ;
#501=DIRECTION ( 'NONE',  ( -6.409494854920720919E-30, 0.8660254037844380415, -0.5000000000000009992 ) ) ;
#507=CARTESIAN_POINT ( 'NONE',  ( 0.000000000000000000, 0.000000000000000000, 0.000000000000000000 ) ) ;
#566=CARTESIAN_POINT ( 'NONE',  ( 4.000000000000003553, -1.759474945355333109, 3.047500000000091802 ) ) ;
#600=FACE_OUTER_BOUND ( 'NONE', #8283, .T. ) ;
#609=AXIS2_PLACEMENT_3D ( 'NONE', #6883, #912, #953 ) ;
#631=CARTESIAN_POINT ( 'NONE',  ( -31.74999999999994316, 4.898587196589875298E-16, -4.000000000000030198 ) ) ;
#654=DIRECTION ( 'NONE',  ( 0.000000000000000000, -1.064348848528640545E-29, 1.000000000000000000 ) ) ;
#660=DIRECTION ( 'NONE',  ( 0.000000000000000000, 1.064348848528640545E-29, -1.000000000000000000 ) ) ;
#693=AXIS2_PLACEMENT_3D ( 'NONE', #6436, #3122, #5806 ) ;
#698=VERTEX_POINT ( 'NONE', #7008 ) ;
#728=DIRECTION ( 'NONE',  ( 0.000000000000000000, -1.042965139114318396E-29, 1.000000000000000000 ) ) ;
#733=VECTOR ( 'NONE', #5528, 1000.000000000000114 ) ;
#740=DIRECTION ( 'NONE',  ( -1.000000000000000000, 3.549874073494553124E-30, 0.000000000000000000 ) ) ;
#744=CARTESIAN_POINT ( 'NONE',  ( 8.000000000000014211, -5.551115123125777653E-14, -4.399999999999364420 ) ) ;
#780=VECTOR ( 'NONE', #1375, 1000.000000000000000 ) ;
#821=AXIS2_PLACEMENT_3D ( 'NONE', #4827, #204, #4216 ) ;
#824=ADVANCED_FACE ( 'NONE', ( #3179 ), #7838, .T. ) ;
#834=DIRECTION ( 'NONE',  ( 0.000000000000000000, -1.064348848528640685E-29, 1.000000000000000000 ) ) ;
#836=ORIENTED_EDGE ( 'NONE', *, *, #4162, .F. ) ;
#856=EDGE_CURVE ( 'NONE', #7966, #872, #2830, .T. ) ;
#863=VERTEX_POINT ( 'NONE', #6533 ) ;
#865=CARTESIAN_POINT ( 'NONE',  ( 4.000000000000058620, 3.518949890710762585, 2.220446049250313081E-13 ) ) ;
#866=EDGE_CURVE ( 'NONE', #7532, #232, #8297, .T. ) ;
#870=ORIENTED_EDGE ( 'NONE', *, *, #7065, .F. ) ;
#872=VERTEX_POINT ( 'NONE', #5909 ) ;
#878=DIRECTION ( 'NONE',  ( 0.000000000000000000, -1.064348848528640545E-29, 1.000000000000000000 ) ) ;
#882=ADVANCED_FACE ( 'NONE', ( #3309 ), #7278, .T. ) ;
#885=CONICAL_SURFACE ( 'NONE', #2968, 3.309499999999999886, 0.7853981633975651855 ) ;
#896=VERTEX_POINT ( 'NONE', #744 ) ;
#905=ORIENTED_EDGE ( 'NONE', *, *, #2015, .F. ) ;
#909=CARTESIAN_POINT ( 'NONE',  ( 4.000000000000003553, 1.759474945355415931, -3.047500000000091802 ) ) ;
#912=DIRECTION ( 'NONE',  ( 1.000000000000000000, -3.549874073494553124E-30, 0.000000000000000000 ) ) ;
#918=DIRECTION ( 'NONE',  ( -1.000000000000000000, 3.549874073494553124E-30, 0.000000000000000000 ) ) ;
#927=VERTEX_POINT ( 'NONE', #4267 ) ;
#934=ORIENTED_EDGE ( 'NONE', *, *, #8009, .T. ) ;
#936=EDGE_LOOP ( 'NONE', ( #4047, #6895, #1027, #2165 ) ) ;
#943=EDGE_CURVE ( 'NONE', #4339, #7532, #6205, .T. ) ;
#949=DIRECTION ( 'NONE',  ( 4.141519752410311978E-30, 8.626909098572831859E-16, 1.000000000000000000 ) ) ;
#953=DIRECTION ( 'NONE',  ( 0.000000000000000000, 1.064348848528640405E-29, -1.000000000000000000 ) ) ;
#954=ORIENTED_EDGE ( 'NONE', *, *, #8456, .T. ) ;
#971=ORIENTED_EDGE ( 'NONE', *, *, #6812, .T. ) ;
#994=PLANE ( 'NONE',  #6434 ) ;
#997=CARTESIAN_POINT ( 'NONE',  ( 8.000000000000007105, 2.775557561562891351E-14, 6.661338147750939243E-13 ) ) ;
#998=FACE_OUTER_BOUND ( 'NONE', #936, .T. ) ;
#1002=CARTESIAN_POINT ( 'NONE',  ( 4.000000000000003553, -1.759474945355339992, -3.047499999999869758 ) ) ;
#1009=DIRECTION ( 'NONE',  ( -1.000000000000000000, 3.549874073494553124E-30, 0.000000000000000000 ) ) ;
#1018=FACE_OUTER_BOUND ( 'NONE', #6088, .T. ) ;
#1021=CIRCLE ( 'NONE', #7137, 3.047499999999999876 ) ;
#1024=ORIENTED_EDGE ( 'NONE', *, *, #7065, .T. ) ;
#1027=ORIENTED_EDGE ( 'NONE', *, *, #144, .T. ) ;
#1030=APPLICATION_CONTEXT ( 'automotive_design' ) ;
#1031=FACE_OUTER_BOUND ( 'NONE', #1567, .T. ) ;
#1039=LINE ( 'NONE', #6358, #7132 ) ;
#1040=DIRECTION ( 'NONE',  ( -1.000000000000000000, 3.549874073494553124E-30, 0.000000000000000000 ) ) ;
#1065=CIRCLE ( 'NONE', #7877, 5.700000000000001954 ) ;
#1074=DIRECTION ( 'NONE',  ( -1.000000000000000000, 3.549874073494553124E-30, 0.000000000000000000 ) ) ;
#1081=CARTESIAN_POINT ( 'NONE',  ( 4.000000000000058620, 3.518949890710762585, 2.220446049250313081E-13 ) ) ;
#1088=EDGE_LOOP ( 'NONE', ( #2286, #7303, #3156, #836 ) ) ;
#1089=EDGE_LOOP ( 'NONE', ( #1523, #8174, #4178, #8253, #3250 ) ) ;
#1092=CARTESIAN_POINT ( 'NONE',  ( 33.00000000000055422, -1.431146867680865853E-14, 6.883382752675970551E-12 ) ) ;
#1145=AXIS2_PLACEMENT_3D ( 'NONE', #2007, #3490, #6118 ) ;
#1151=LINE ( 'NONE', #334, #6858 ) ;
#1179=PRODUCT ( 'socket head cap screw_am_B18.3.1M - 8 x 1.25 x 25 Hex SHCS -- 25NHX', 'socket head cap screw_am_B18.3.1M - 8 x 1.25 x 25 Hex SHCS -- 25NHX', '', ( #1697 ) ) ;
#1196=CARTESIAN_POINT ( 'NONE',  ( 4.000000000000003553, 1.759474945355415931, -3.047500000000091802 ) ) ;
#1209=ORIENTED_EDGE ( 'NONE', *, *, #3887, .T. ) ;
#1212=CARTESIAN_POINT ( 'NONE',  ( 4.000000000000003553, 1.759474945355374409, 3.047499999999869758 ) ) ;
#1215=DIRECTION ( 'NONE',  ( 0.000000000000000000, -1.042965139114318115E-29, 1.000000000000000000 ) ) ;
#1219=VERTEX_POINT ( 'NONE', #440 ) ;
#1225=( NAMED_UNIT ( * ) SI_UNIT ( $, .STERADIAN. ) SOLID_ANGLE_UNIT ( ) );
#1258=LINE ( 'NONE', #1402, #6863 ) ;
#1264=DIRECTION ( 'NONE',  ( -1.000000000000000000, 3.549874073494553124E-30, 3.778304382545602261E-59 ) ) ;
#1284=CARTESIAN_POINT ( 'NONE',  ( 4.000000000000003553, 1.759474945355415931, -3.047500000000091802 ) ) ;
#1288=ORIENTED_EDGE ( 'NONE', *, *, #153, .F. ) ;
#1293=AXIS2_PLACEMENT_3D ( 'NONE', #1876, #7191, #1215 ) ;
#1301=ADVANCED_FACE ( 'NONE', ( #5308 ), #5261, .T. ) ;
#1304=ORIENTED_EDGE ( 'NONE', *, *, #8456, .F. ) ;
#1305=ORIENTED_EDGE ( 'NONE', *, *, #108, .T. ) ;
#1306=VECTOR ( 'NONE', #3279, 1000.000000000000000 ) ;
#1309=ORIENTED_EDGE ( 'NONE', *, *, #5469, .F. ) ;
#1316=ORIENTED_EDGE ( 'NONE', *, *, #7500, .T. ) ;
#1338=CARTESIAN_POINT ( 'NONE',  ( 8.000000000000007105, 2.775557561562891351E-14, 6.661338147750939243E-13 ) ) ;
#1371=ADVANCED_FACE ( 'NONE', ( #1596 ), #244, .F. ) ;
#1373=LINE ( 'NONE', #3940, #7807 ) ;
#1375=DIRECTION ( 'NONE',  ( 3.549874073494553825E-30, -1.000000000000000000, 1.478898702612476446E-15 ) ) ;
#1387=AXIS2_PLACEMENT_3D ( 'NONE', #1493, #6131, #138 ) ;
#1395=AXIS2_PLACEMENT_3D ( 'NONE', #5615, #4855, #2986 ) ;
#1398=ORIENTED_EDGE ( 'NONE', *, *, #4013, .T. ) ;
#1402=CARTESIAN_POINT ( 'NONE',  ( 33.00000000000055422, -1.390617181863080626E-14, -3.309499999993116504 ) ) ;
#1407=AXIS2_PLACEMENT_3D ( 'NONE', #4355, #1009, #878 ) ;
#1410=ADVANCED_FACE ( 'NONE', ( #1631 ), #6923, .F. ) ;
#1421=ORIENTED_EDGE ( 'NONE', *, *, #4196, .F. ) ;
#1425=EDGE_CURVE ( 'NONE', #6623, #6876, #4129, .T. ) ;
#1459=ORIENTED_EDGE ( 'NONE', *, *, #1505, .F. ) ;
#1493=CARTESIAN_POINT ( 'NONE',  ( 8.000000000000007105, 2.775557561562891351E-14, 6.661338147750939243E-13 ) ) ;
#1496=VERTEX_POINT ( 'NONE', #3849 ) ;
#1498=EDGE_CURVE ( 'NONE', #2701, #1642, #3574, .T. ) ;
#1505=EDGE_CURVE ( 'NONE', #6208, #8158, #1065, .T. ) ;
#1523=ORIENTED_EDGE ( 'NONE', *, *, #2717, .F. ) ;
#1543=EDGE_LOOP ( 'NONE', ( #4292, #90, #7103, #321, #2523 ) ) ;
#1551=DIRECTION ( 'NONE',  ( -1.000000000000000000, 3.549874073494553124E-30, 0.000000000000000000 ) ) ;
#1567=EDGE_LOOP ( 'NONE', ( #1398, #8035, #25, #870, #250 ) ) ;
#1588=EDGE_LOOP ( 'NONE', ( #5037, #2920, #4876, #7419 ) ) ;
#1596=FACE_OUTER_BOUND ( 'NONE', #1543, .T. ) ;
#1597=CARTESIAN_POINT ( 'NONE',  ( 0.000000000000000000, 0.000000000000000000, 0.000000000000000000 ) ) ;
#1628=CARTESIAN_POINT ( 'NONE',  ( 4.000000000000003553, -1.759474945355333109, 3.047500000000091802 ) ) ;
#1631=FACE_OUTER_BOUND ( 'NONE', #2344, .T. ) ;
#1638=ORIENTED_EDGE ( 'NONE', *, *, #2321, .F. ) ;
#1642=VERTEX_POINT ( 'NONE', #8466 ) ;
#1674=DIRECTION ( 'NONE',  ( 0.000000000000000000, -1.064348848528640405E-29, 1.000000000000000000 ) ) ;
#1675=LINE ( 'NONE', #5490, #4722 ) ;
#1694=AXIS2_PLACEMENT_3D ( 'NONE', #3504, #6179, #5519 ) ;
#1697=PRODUCT_CONTEXT ( 'NONE', #4636, 'mechanical' ) ;
#1702=CARTESIAN_POINT ( 'NONE',  ( 33.00000000000055422, -1.431146867680865853E-14, 6.883382752675970551E-12 ) ) ;
#1705=DIRECTION ( 'NONE',  ( -6.310887241768093743E-30, 0.8660254037844380415, -0.5000000000000009992 ) ) ;
#1712=VERTEX_POINT ( 'NONE', #7296 ) ;
#1721=CARTESIAN_POINT ( 'NONE',  ( 4.000000000000003553, 0.000000000000000000, -3.047500000000091802 ) ) ;
#1723=DIRECTION ( 'NONE',  ( -3.549874073494553124E-30, 1.000000000000000000, -8.626909098572831859E-16 ) ) ;
#1754=EDGE_LOOP ( 'NONE', ( #8464, #3278, #5220, #7979, #3112 ) ) ;
#1783=ORIENTED_EDGE ( 'NONE', *, *, #7377, .T. ) ;
#1787=AXIS2_PLACEMENT_3D ( 'NONE', #4130, #6022, #3257 ) ;
#1793=DIRECTION ( 'NONE',  ( -3.549874073494553124E-30, 0.5000000000000009992, 0.8660254037844380415 ) ) ;
#1819=LINE ( 'NONE', #5856, #5989 ) ;
#1843=CIRCLE ( 'NONE', #5629, 0.4000000000000001887 ) ;
#1844=DIRECTION ( 'NONE',  ( -1.000000000000000000, 3.549874073494553124E-30, 0.000000000000000000 ) ) ;
#1857=DIRECTION ( 'NONE',  ( -1.000000000000000000, 3.549874073494553124E-30, 0.000000000000000000 ) ) ;
#1876=CARTESIAN_POINT ( 'NONE',  ( 0.7999999999999674039, -1.387778780781445676E-14, 0.000000000000000000 ) ) ;
#1887=EDGE_LOOP ( 'NONE', ( #4243, #5608 ) ) ;
#1914=ORIENTED_EDGE ( 'NONE', *, *, #6448, .F. ) ;
#1915=CARTESIAN_POINT ( 'NONE',  ( 4.000000000000003553, 9.714451465470119729E-14, 0.000000000000000000 ) ) ;
#1928=LINE ( 'NONE', #4589, #114 ) ;
#1943=CONICAL_SURFACE ( 'NONE', #2642, 3.047499999999999876, 1.047197551196592524 ) ;
#1947=FACE_OUTER_BOUND ( 'NONE', #236, .T. ) ;
#1991=AXIS2_PLACEMENT_3D ( 'NONE', #3266, #6715, #8574 ) ;
#2007=CARTESIAN_POINT ( 'NONE',  ( 4.000000000000003553, 9.714451465470119729E-14, 0.000000000000000000 ) ) ;
#2014=ORIENTED_EDGE ( 'NONE', *, *, #4013, .F. ) ;
#2015=EDGE_CURVE ( 'NONE', #232, #3217, #6423, .T. ) ;
#2029=ADVANCED_FACE ( 'NONE', ( #1031 ), #6308, .F. ) ;
#2047=DIRECTION ( 'NONE',  ( 1.000000000000000000, -3.549874073494553124E-30, -3.778304382545602261E-59 ) ) ;
#2055=ORIENTED_EDGE ( 'NONE', *, *, #6812, .F. ) ;
#2060=CIRCLE ( 'NONE', #4573, 4.000000000000030198 ) ;
#2081=CIRCLE ( 'NONE', #1787, 3.309499999999999886 ) ;
#2096=EDGE_LOOP ( 'NONE', ( #7375, #4336 ) ) ;
#2117=CARTESIAN_POINT ( 'NONE',  ( 0.7999999999999674039, 7.960204194457039156E-16, 6.499999999999968026 ) ) ;
#2125=ORIENTED_EDGE ( 'NONE', *, *, #2156, .T. ) ;
#2129=AXIS2_PLACEMENT_3D ( 'NONE', #1915, #740, #6529 ) ;
#2134=ORIENTED_EDGE ( 'NONE', *, *, #2890, .T. ) ;
#2154=VECTOR ( 'NONE', #7172, 1000.000000000000000 ) ;
#2156=EDGE_CURVE ( 'NONE', #927, #7841, #1928, .T. ) ;
#2165=ORIENTED_EDGE ( 'NONE', *, *, #8332, .T. ) ;
#2179=DIRECTION ( 'NONE',  ( 3.549874073494553124E-30, -0.5000000000000009992, -0.8660254037844380415 ) ) ;
#2184=DIRECTION ( 'NONE',  ( -0.5000000000000044409, -7.442594376397861402E-30, 0.8660254037844360431 ) ) ;
#2224=VECTOR ( 'NONE', #5858, 1000.000000000000000 ) ;
#2267=VECTOR ( 'NONE', #1844, 1000.000000000000000 ) ;
#2269=CIRCLE ( 'NONE', #1694, 6.500000000000002665 ) ;
#2285=EDGE_CURVE ( 'NONE', #2701, #3620, #404, .T. ) ;
#2286=ORIENTED_EDGE ( 'NONE', *, *, #8009, .F. ) ;
#2304=FACE_OUTER_BOUND ( 'NONE', #7, .T. ) ;
#2321=EDGE_CURVE ( 'NONE', #7532, #173, #259, .T. ) ;
#2322=DIRECTION ( 'NONE',  ( -1.000000000000000000, 3.549874073494553124E-30, 0.000000000000000000 ) ) ;
#2330=DIRECTION ( 'NONE',  ( -1.000000000000000000, 3.549874073494553124E-30, -0.000000000000000000 ) ) ;
#2344=EDGE_LOOP ( 'NONE', ( #6733, #905, #8425, #1309, #3615 ) ) ;
#2366=VECTOR ( 'NONE', #2909, 1000.000000000000000 ) ;
#2378=DIRECTION ( 'NONE',  ( 1.000000000000000000, -3.549874073494553124E-30, 0.000000000000000000 ) ) ;
#2399=DIRECTION ( 'NONE',  ( 0.000000000000000000, -1.213383262747659708E-29, 1.000000000000000000 ) ) ;
#2407=CARTESIAN_POINT ( 'NONE',  ( 8.400000000000018119, 4.898587196541454030E-16, -3.999999999999364508 ) ) ;
#2414=ORIENTED_EDGE ( 'NONE', *, *, #2717, .T. ) ;
#2425=DIRECTION ( 'NONE',  ( -3.549874073494553124E-30, 1.000000000000000000, -8.626909098572831859E-16 ) ) ;
#2443=CARTESIAN_POINT ( 'NONE',  ( 32.30950000000065359, -4.257395394114627200E-29, 4.000000000006943779 ) ) ;
#2463=CYLINDRICAL_SURFACE ( 'NONE', #8529, 6.500000000000001776 ) ;
#2483=DIRECTION ( 'NONE',  ( 0.000000000000000000, -1.064348848528640545E-29, 1.000000000000000000 ) ) ;
#2492=CARTESIAN_POINT ( 'NONE',  ( 4.000000000000058620, 3.518949890710762585, 2.220446049250313081E-13 ) ) ;
#2501=LINE ( 'NONE', #5151, #2267 ) ;
#2507=DIRECTION ( 'NONE',  ( 0.000000000000000000, -1.024214141749972931E-29, 1.000000000000000000 ) ) ;
#2517=EDGE_CURVE ( 'NONE', #896, #4276, #7229, .T. ) ;
#2523=ORIENTED_EDGE ( 'NONE', *, *, #6074, .T. ) ;
#2528=DIRECTION ( 'NONE',  ( -1.000000000000000000, 3.549874073494553124E-30, 3.778304382545602261E-59 ) ) ;
#2529=VECTOR ( 'NONE', #4259, 1000.000000000000000 ) ;
#2600=PLANE ( 'NONE',  #4361 ) ;
#2627=CARTESIAN_POINT ( 'NONE',  ( 4.000000000000003553, 9.714451465470119729E-14, 0.000000000000000000 ) ) ;
#2642=AXIS2_PLACEMENT_3D ( 'NONE', #5419, #3545, #4844 ) ;
#2701=VERTEX_POINT ( 'NONE', #116 ) ;
#2711=CARTESIAN_POINT ( 'NONE',  ( -31.74999999999994316, -4.257395394114594689E-29, 4.000000000000030198 ) ) ;
#2717=EDGE_CURVE ( 'NONE', #5352, #3689, #6025, .T. ) ;
#2754=ORIENTED_EDGE ( 'NONE', *, *, #3471, .F. ) ;
#2781=CARTESIAN_POINT ( 'NONE',  ( 5.551115123125782702E-14, 3.518949890710790118, 2.220446049250313081E-13 ) ) ;
#2783=ORIENTED_EDGE ( 'NONE', *, *, #2793, .F. ) ;
#2790=CARTESIAN_POINT ( 'NONE',  ( 0.000000000000000000, -3.518949890710769690, 0.000000000000000000 ) ) ;
#2791=STYLED_ITEM('',(#8670),#5753);
#2793=EDGE_CURVE ( 'NONE', #1712, #3620, #432, .T. ) ;
#2813=CARTESIAN_POINT ( 'NONE',  ( 8.000000000000007105, 2.775557561562884725E-14, 6.500000000000667022 ) ) ;
#2829=EDGE_LOOP ( 'NONE', ( #3556, #7576 ) ) ;
#2830=CIRCLE ( 'NONE', #1293, 6.500000000000002665 ) ;
#2841=CIRCLE ( 'NONE', #3794, 4.400000000000030553 ) ;
#2842=AXIS2_PLACEMENT_3D ( 'NONE', #3781, #2378, #7776 ) ;
#2843=FACE_OUTER_BOUND ( 'NONE', #6654, .T. ) ;
#2863=DIRECTION ( 'NONE',  ( 3.733809166716685024E-60, -1.478898702612462838E-15, -1.000000000000000000 ) ) ;
#2883=CARTESIAN_POINT ( 'NONE',  ( -31.74999999999994316, 7.960204194458489674E-16, -6.500000000000001776 ) ) ;
#2890=EDGE_CURVE ( 'NONE', #6876, #3217, #2999, .T. ) ;
#2903=CARTESIAN_POINT ( 'NONE',  ( 4.000000000000003553, -1.759474945355333109, 3.047500000000091802 ) ) ;
#2909=DIRECTION ( 'NONE',  ( 0.000000000000000000, -0.4999999999999983902, 0.8660254037844395958 ) ) ;
#2920=ORIENTED_EDGE ( 'NONE', *, *, #445, .T. ) ;
#2923=CIRCLE ( 'NONE', #7239, 3.047499999999999876 ) ;
#2938=VERTEX_POINT ( 'NONE', #8399 ) ;
#2965=ORIENTED_EDGE ( 'NONE', *, *, #7217, .T. ) ;
#2968=AXIS2_PLACEMENT_3D ( 'NONE', #1092, #3052, #8369 ) ;
#2986=DIRECTION ( 'NONE',  ( 0.000000000000000000, 1.540743955509787842E-29, -1.000000000000000000 ) ) ;
#2999=LINE ( 'NONE', #249, #2366 ) ;
#3018=CARTESIAN_POINT ( 'NONE',  ( 8.400000000000018119, -5.497230663963303402E-14, 4.400000000000696687 ) ) ;
#3029=LINE ( 'NONE', #1628, #8246 ) ;
#3045=FACE_BOUND ( 'NONE', #8495, .T. ) ;
#3052=DIRECTION ( 'NONE',  ( -1.000000000000000000, 3.549874073494553124E-30, 0.000000000000000000 ) ) ;
#3053=PLANE ( 'NONE',  #8241 ) ;
#3062=CARTESIAN_POINT ( 'NONE',  ( 4.000000000000003553, 9.714451465470119729E-14, 0.000000000000000000 ) ) ;
#3074=CARTESIAN_POINT ( 'NONE',  ( 0.000000000000000000, -1.759474945355326225, -3.047499999999869758 ) ) ;
#3080=ADVANCED_FACE ( 'NONE', ( #8264 ), #994, .T. ) ;
#3095=AXIS2_PLACEMENT_3D ( 'NONE', #1702, #6951, #7718 ) ;
#3107=ADVANCED_FACE ( 'NONE', ( #6710 ), #6719, .F. ) ;
#3112=ORIENTED_EDGE ( 'NONE', *, *, #7757, .T. ) ;
#3113=DIRECTION ( 'NONE',  ( 0.000000000000000000, -0.5000000000000009992, -0.8660254037844380415 ) ) ;
#3121=DIRECTION ( 'NONE',  ( 0.7071067811865483499, 8.659560562353920898E-17, 0.7071067811865467956 ) ) ;
#3122=DIRECTION ( 'NONE',  ( -1.000000000000000000, 3.549874073494553124E-30, 0.000000000000000000 ) ) ;
#3128=ADVANCED_FACE ( 'NONE', ( #3911, #6574 ), #8530, .T. ) ;
#3129=VECTOR ( 'NONE', #2425, 1000.000000000000000 ) ;
#3156=ORIENTED_EDGE ( 'NONE', *, *, #3840, .T. ) ;
#3179=FACE_OUTER_BOUND ( 'NONE', #4897, .T. ) ;
#3187=DIRECTION ( 'NONE',  ( -1.000000000000000000, 3.549874073494553124E-30, 0.000000000000000000 ) ) ;
#3217=VERTEX_POINT ( 'NONE', #3578 ) ;
#3233=AXIS2_PLACEMENT_3D ( 'NONE', #6716, #31, #660 ) ;
#3240=PRODUCT_DEFINITION_CONTEXT ( 'detailed design', #1030, 'design' ) ;
#3250=ORIENTED_EDGE ( 'NONE', *, *, #3471, .T. ) ;
#3257=DIRECTION ( 'NONE',  ( 0.000000000000000000, -1.024214141749972931E-29, 1.000000000000000000 ) ) ;
#3261=DIRECTION ( 'NONE',  ( 0.000000000000000000, 1.064348848528640545E-29, -1.000000000000000000 ) ) ;
#3266=CARTESIAN_POINT ( 'NONE',  ( 0.000000000000000000, 0.000000000000000000, 0.000000000000000000 ) ) ;
#3278=ORIENTED_EDGE ( 'NONE', *, *, #943, .T. ) ;
#3279=DIRECTION ( 'NONE',  ( -1.000000000000000000, 3.549874073494553124E-30, 0.000000000000000000 ) ) ;
#3283=LINE ( 'NONE', #4604, #8475 ) ;
#3294=DIRECTION ( 'NONE',  ( 0.000000000000000000, -0.4999999999999987232, 0.8660254037844393737 ) ) ;
#3309=FACE_OUTER_BOUND ( 'NONE', #3784, .T. ) ;
#3312=ORIENTED_EDGE ( 'NONE', *, *, #445, .F. ) ;
#3316=DIRECTION ( 'NONE',  ( 3.549874073494553124E-30, -0.5000000000000009992, -0.8660254037844380415 ) ) ;
#3379=CARTESIAN_POINT ( 'NONE',  ( 0.000000000000000000, -1.759474945355374631, 3.047500000000091802 ) ) ;
#3395=DIRECTION ( 'NONE',  ( 0.000000000000000000, -0.5000000000000009992, -0.8660254037844380415 ) ) ;
#3399=ORIENTED_EDGE ( 'NONE', *, *, #3887, .F. ) ;
#3406=PLANE ( 'NONE',  #3233 ) ;
#3426=DIRECTION ( 'NONE',  ( 3.646298014371739284E-59, 1.027162637006519249E-29, -1.000000000000000000 ) ) ;
#3429=ORIENTED_EDGE ( 'NONE', *, *, #144, .F. ) ;
#3447=( NAMED_UNIT ( * ) PLANE_ANGLE_UNIT ( ) SI_UNIT ( $, .RADIAN. ) );
#3459=ORIENTED_EDGE ( 'NONE', *, *, #6854, .T. ) ;
#3461=EDGE_CURVE ( 'NONE', #863, #7532, #8509, .T. ) ;
#3471=EDGE_CURVE ( 'NONE', #5176, #3689, #2501, .T. ) ;
#3475=DIRECTION ( 'NONE',  ( -3.549874073494553124E-30, 1.000000000000000000, -1.478898702612462838E-15 ) ) ;
#3490=DIRECTION ( 'NONE',  ( -1.000000000000000000, 3.549874073494553124E-30, 0.000000000000000000 ) ) ;
#3504=CARTESIAN_POINT ( 'NONE',  ( 0.7999999999999674039, -1.387778780781445676E-14, 0.000000000000000000 ) ) ;
#3512=DIRECTION ( 'NONE',  ( 1.000000000000000000, 0.000000000000000000, 0.000000000000000000 ) ) ;
#3540=CARTESIAN_POINT ( 'NONE',  ( 4.000000000000003553, 1.759474945355374409, 3.047499999999869758 ) ) ;
#3545=DIRECTION ( 'NONE',  ( -1.000000000000000000, 3.549874073494553124E-30, 0.000000000000000000 ) ) ;
#3556=ORIENTED_EDGE ( 'NONE', *, *, #1498, .F. ) ;
#3568=LINE ( 'NONE', #2711, #7680 ) ;
#3574=CIRCLE ( 'NONE', #8432, 3.309499999999999886 ) ;
#3578=CARTESIAN_POINT ( 'NONE',  ( 0.000000000000000000, 1.759474945355318898, 3.047499999999869758 ) ) ;
#3606=LINE ( 'NONE', #6796, #7671 ) ;
#3615=ORIENTED_EDGE ( 'NONE', *, *, #177, .T. ) ;
#3620=VERTEX_POINT ( 'NONE', #2443 ) ;
#3641=ADVANCED_FACE ( 'NONE', ( #4488 ), #8496, .T. ) ;
#3659=DIRECTION ( 'NONE',  ( -1.000000000000000000, 3.549874073494553124E-30, 0.000000000000000000 ) ) ;
#3668=AXIS2_PLACEMENT_3D ( 'NONE', #7752, #2528, #7885 ) ;
#3675=CONICAL_SURFACE ( 'NONE', #609, 5.700000000000001954, 0.7853981633974472798 ) ;
#3689=VERTEX_POINT ( 'NONE', #7890 ) ;
#3702=DIRECTION ( 'NONE',  ( 1.000000000000000000, -3.549874073494553124E-30, 0.000000000000000000 ) ) ;
#3711=ORIENTED_EDGE ( 'NONE', *, *, #2517, .F. ) ;
#3728=ORIENTED_EDGE ( 'NONE', *, *, #8498, .F. ) ;
#3774=EDGE_CURVE ( 'NONE', #5857, #863, #7391, .T. ) ;
#3781=CARTESIAN_POINT ( 'NONE',  ( 8.400000000000018119, -5.551115123125782702E-14, 6.661338147750939243E-13 ) ) ;
#3784=EDGE_LOOP ( 'NONE', ( #8265, #1459, #1783, #8545 ) ) ;
#3793=EDGE_CURVE ( 'NONE', #863, #5176, #3029, .T. ) ;
#3794=AXIS2_PLACEMENT_3D ( 'NONE', #997, #2330, #8387 ) ;
#3809=CARTESIAN_POINT ( 'NONE',  ( 4.000000000000003553, 9.714451465470119729E-14, 0.000000000000000000 ) ) ;
#3824=EDGE_CURVE ( 'NONE', #4276, #896, #2841, .T. ) ;
#3828=CARTESIAN_POINT ( 'NONE',  ( 4.000000000000003553, -1.759474945355339992, -3.047499999999869758 ) ) ;
#3840=EDGE_CURVE ( 'NONE', #7453, #7966, #1151, .T. ) ;
#3849=CARTESIAN_POINT ( 'NONE',  ( 0.000000000000000000, 1.759474945355512965, -3.047500000000091802 ) ) ;
#3850=CARTESIAN_POINT ( 'NONE',  ( 4.000000000000003553, -1.759474945355333109, 3.047500000000091802 ) ) ;
#3866=ORIENTED_EDGE ( 'NONE', *, *, #5774, .F. ) ;
#3887=EDGE_CURVE ( 'NONE', #5176, #698, #1039, .T. ) ;
#3911=FACE_BOUND ( 'NONE', #2096, .T. ) ;
#3925=CONICAL_SURFACE ( 'NONE', #3095, 3.309499999999999886, 0.7853981633975651855 ) ;
#3940=CARTESIAN_POINT ( 'NONE',  ( 4.000000000000003553, 9.751772576674139373E-14, -3.047499999999999876 ) ) ;
#3945=ADVANCED_FACE ( 'NONE', ( #5203 ), #4505, .T. ) ;
#3949=ORIENTED_EDGE ( 'NONE', *, *, #866, .T. ) ;
#3963=ORIENTED_EDGE ( 'NONE', *, *, #5774, .T. ) ;
#3982=ORIENTED_EDGE ( 'NONE', *, *, #3793, .F. ) ;
#4013=EDGE_CURVE ( 'NONE', #6876, #1496, #5293, .T. ) ;
#4030=CIRCLE ( 'NONE', #1395, 0.4000000000000001887 ) ;
#4038=EDGE_LOOP ( 'NONE', ( #6325, #5378, #3711, #4893 ) ) ;
#4047=ORIENTED_EDGE ( 'NONE', *, *, #4048, .F. ) ;
#4048=EDGE_CURVE ( 'NONE', #1712, #4183, #6599, .T. ) ;
#4078=AXIS2_PLACEMENT_3D ( 'NONE', #3809, #6466, #5837 ) ;
#4101=ORIENTED_EDGE ( 'NONE', *, *, #3461, .F. ) ;
#4129=LINE ( 'NONE', #865, #5223 ) ;
#4130=CARTESIAN_POINT ( 'NONE',  ( 33.00000000000055422, -1.431146867680865853E-14, 6.883382752675970551E-12 ) ) ;
#4162=EDGE_CURVE ( 'NONE', #872, #7966, #2269, .T. ) ;
#4166=CARTESIAN_POINT ( 'NONE',  ( 4.000000000000003553, -1.759474945355333109, 3.047500000000091802 ) ) ;
#4176=VECTOR ( 'NONE', #3395, 1000.000000000000114 ) ;
#4178=ORIENTED_EDGE ( 'NONE', *, *, #3774, .T. ) ;
#4183=VERTEX_POINT ( 'NONE', #2407 ) ;
#4196=EDGE_CURVE ( 'NONE', #5835, #698, #1021, .T. ) ;
#4203=CARTESIAN_POINT ( 'NONE',  ( 0.000000000000000000, 0.000000000000000000, 0.000000000000000000 ) ) ;
#4213=EDGE_CURVE ( 'NONE', #2938, #4276, #1843, .T. ) ;
#4216=DIRECTION ( 'NONE',  ( 3.646298014371739284E-59, 1.027162637006519249E-29, -1.000000000000000000 ) ) ;
#4217=FACE_OUTER_BOUND ( 'NONE', #325, .T. ) ;
#4231=EDGE_LOOP ( 'NONE', ( #5522, #3728, #1316, #5962 ) ) ;
#4233=AXIS2_PLACEMENT_3D ( 'NONE', #5153, #7901, #6643 ) ;
#4234=( GEOMETRIC_REPRESENTATION_CONTEXT ( 3 ) GLOBAL_UNCERTAINTY_ASSIGNED_CONTEXT ( ( #7167 ) ) GLOBAL_UNIT_ASSIGNED_CONTEXT ( ( #7330, #5421, #1225 ) ) REPRESENTATION_CONTEXT ( 'NONE', 'WORKASPACE' ) );
#4243=ORIENTED_EDGE ( 'NONE', *, *, #1505, .T. ) ;
#4247=ADVANCED_FACE ( 'NONE', ( #7882 ), #3925, .T. ) ;
#4259=DIRECTION ( 'NONE',  ( -1.000000000000000000, 3.549874073494553124E-30, 0.000000000000000000 ) ) ;
#4267=CARTESIAN_POINT ( 'NONE',  ( 4.000000000000003553, 2.639212418032998997, -1.523749999999823856 ) ) ;
#4275=DIRECTION ( 'NONE',  ( -1.000000000000000000, 3.549874073494553124E-30, 0.000000000000000000 ) ) ;
#4276=VERTEX_POINT ( 'NONE', #5609 ) ;
#4284=DIRECTION ( 'NONE',  ( -1.000000000000000000, 3.549874073494553124E-30, 0.000000000000000000 ) ) ;
#4287=ORIENTED_EDGE ( 'NONE', *, *, #4995, .T. ) ;
#4292=ORIENTED_EDGE ( 'NONE', *, *, #7389, .T. ) ;
#4324=ORIENTED_EDGE ( 'NONE', *, *, #5469, .T. ) ;
#4334=VECTOR ( 'NONE', #5913, 1000.000000000000000 ) ;
#4336=ORIENTED_EDGE ( 'NONE', *, *, #3824, .T. ) ;
#4339=VERTEX_POINT ( 'NONE', #6077 ) ;
#4342=DIRECTION ( 'NONE',  ( 0.000000000000000000, -1.064348848528640405E-29, 1.000000000000000000 ) ) ;
#4355=CARTESIAN_POINT ( 'NONE',  ( -31.74999999999994316, 0.000000000000000000, 0.000000000000000000 ) ) ;
#4361=AXIS2_PLACEMENT_3D ( 'NONE', #5258, #6611, #3294 ) ;
#4416=ORIENTED_EDGE ( 'NONE', *, *, #7757, .F. ) ;
#4435=AXIS2_PLACEMENT_3D ( 'NONE', #8372, #4275, #2399 ) ;
#4462=ADVANCED_FACE ( 'NONE', ( #600 ), #2600, .T. ) ;
#4468=DIRECTION ( 'NONE',  ( -1.000000000000000000, 3.549874073494553124E-30, 0.000000000000000000 ) ) ;
#4474=DIRECTION ( 'NONE',  ( 0.000000000000000000, 0.4999999999999986677, -0.8660254037844393737 ) ) ;
#4488=FACE_OUTER_BOUND ( 'NONE', #6418, .T. ) ;
#4505=PLANE ( 'NONE',  #4233 ) ;
#4515=ADVANCED_FACE ( 'NONE', ( #5461 ), #6897, .T. ) ;
#4566=FACE_OUTER_BOUND ( 'NONE', #1887, .T. ) ;
#4573=AXIS2_PLACEMENT_3D ( 'NONE', #8312, #3702, #6281 ) ;
#4575=AXIS2_PLACEMENT_3D ( 'NONE', #6445, #7744, #483 ) ;
#4577=AXIS2_PLACEMENT_3D ( 'NONE', #2492, #1705, #1793 ) ;
#4589=CARTESIAN_POINT ( 'NONE',  ( 4.000000000000058620, 3.518949890710762585, 2.220446049250313081E-13 ) ) ;
#4604=CARTESIAN_POINT ( 'NONE',  ( 0.000000000000000000, 6.066788436613252661E-29, -5.700000000000001954 ) ) ;
#4610=CARTESIAN_POINT ( 'NONE',  ( 4.000000000000003553, 1.759474945355374409, 3.047499999999869758 ) ) ;
#4636=APPLICATION_CONTEXT ( 'automotive_design' ) ;
#4648=VECTOR ( 'NONE', #2184, 1000.000000000000114 ) ;
#4672=CARTESIAN_POINT ( 'NONE',  ( 4.000000000000003553, 1.759474945355415931, -3.047500000000091802 ) ) ;
#4680=ADVANCED_FACE ( 'NONE', ( #2843 ), #885, .T. ) ;
#4687=CARTESIAN_POINT ( 'NONE',  ( 5.551115123125782702E-14, 3.518949890710790118, 2.220446049250313081E-13 ) ) ;
#4698=AXIS2_PLACEMENT_3D ( 'NONE', #4610, #7259, #6655 ) ;
#4708=CARTESIAN_POINT ( 'NONE',  ( 8.000000000000341061, 6.499999999999922728, 8.881784197001252323E-13 ) ) ;
#4719=EDGE_LOOP ( 'NONE', ( #1421, #8540, #2055 ) ) ;
#4722=VECTOR ( 'NONE', #2179, 1000.000000000000000 ) ;
#4747=CARTESIAN_POINT ( 'NONE',  ( -31.74999999999994316, 0.000000000000000000, 0.000000000000000000 ) ) ;
#4776=DIRECTION ( 'NONE',  ( -0.5000000000000044409, 1.060575238725013534E-16, -0.8660254037844360431 ) ) ;
#4825=DIRECTION ( 'NONE',  ( 0.000000000000000000, -0.4999999999999983902, 0.8660254037844395958 ) ) ;
#4827=CARTESIAN_POINT ( 'NONE',  ( 8.400000000000018119, -5.551115123125782702E-14, 6.661338147750939243E-13 ) ) ;
#4834=CARTESIAN_POINT ( 'NONE',  ( 4.000000000000003553, 9.714451465470115942E-14, 3.047499999999999876 ) ) ;
#4841=DIRECTION ( 'NONE',  ( 0.000000000000000000, -1.064348848528640545E-29, 1.000000000000000000 ) ) ;
#4844=DIRECTION ( 'NONE',  ( 0.000000000000000000, -1.213383262747659708E-29, 1.000000000000000000 ) ) ;
#4855=DIRECTION ( 'NONE',  ( -3.549874073494553124E-30, -1.000000000000000000, -1.064348848528640545E-29 ) ) ;
#4871=VECTOR ( 'NONE', #2322, 1000.000000000000000 ) ;
#4876=ORIENTED_EDGE ( 'NONE', *, *, #7217, .F. ) ;
#4880=ORIENTED_EDGE ( 'NONE', *, *, #3840, .F. ) ;
#4893=ORIENTED_EDGE ( 'NONE', *, *, #7500, .F. ) ;
#4897=EDGE_LOOP ( 'NONE', ( #3866, #3399, #3982 ) ) ;
#4910=ADVANCED_FACE ( 'NONE', ( #998 ), #5407, .T. ) ;
#4931=FACE_OUTER_BOUND ( 'NONE', #149, .T. ) ;
#4952=CARTESIAN_POINT ( 'NONE',  ( 4.000000000000003553, 2.639212418033096252, 1.523750000000267946 ) ) ;
#4980=TOROIDAL_SURFACE ( 'NONE', #821, 4.400000000000030553, 0.4000000000000000222 ) ;
#4995=EDGE_CURVE ( 'NONE', #3689, #5847, #122, .T. ) ;
#5004=ADVANCED_FACE ( 'NONE', ( #1947 ), #5215, .T. ) ;
#5010=CARTESIAN_POINT ( 'NONE',  ( 4.000000000000003553, 1.759474945355374409, 3.047499999999869758 ) ) ;
#5036=CARTESIAN_POINT ( 'NONE',  ( -31.74999999999994316, 0.000000000000000000, 0.000000000000000000 ) ) ;
#5037=ORIENTED_EDGE ( 'NONE', *, *, #1498, .T. ) ;
#5068=ORIENTED_EDGE ( 'NONE', *, *, #856, .T. ) ;
#5089=EDGE_CURVE ( 'NONE', #7453, #1219, #6123, .T. ) ;
#5123=VECTOR ( 'NONE', #1723, 1000.000000000000000 ) ;
#5150=ORIENTED_EDGE ( 'NONE', *, *, #5089, .F. ) ;
#5151=CARTESIAN_POINT ( 'NONE',  ( 4.000000000000003553, -3.518949890710769690, 0.000000000000000000 ) ) ;
#5153=CARTESIAN_POINT ( 'NONE',  ( 4.000000000000058620, 3.518949890710762585, 2.220446049250313081E-13 ) ) ;
#5155=CARTESIAN_POINT ( 'NONE',  ( 33.00000000000055422, -1.431146867680865853E-14, 6.883382752675970551E-12 ) ) ;
#5164=AXIS2_PLACEMENT_3D ( 'NONE', #1597, #8024, #1674 ) ;
#5176=VERTEX_POINT ( 'NONE', #6304 ) ;
#5197=CARTESIAN_POINT ( 'NONE',  ( 4.000000000000003553, 1.759474945355415931, -3.047500000000091802 ) ) ;
#5203=FACE_OUTER_BOUND ( 'NONE', #7101, .T. ) ;
#5210=CARTESIAN_POINT ( 'NONE',  ( 0.000000000000000000, -1.759474945355374631, 3.047500000000091802 ) ) ;
#5215=PLANE ( 'NONE',  #4698 ) ;
#5220=ORIENTED_EDGE ( 'NONE', *, *, #2321, .T. ) ;
#5223=VECTOR ( 'NONE', #1551, 1000.000000000000000 ) ;
#5240=DIRECTION ( 'NONE',  ( 0.000000000000000000, -1.042965139114318396E-29, 1.000000000000000000 ) ) ;
#5242=VECTOR ( 'NONE', #5305, 1000.000000000000227 ) ;
#5247=DIRECTION ( 'NONE',  ( 3.549874073494553124E-30, -0.5000000000000009992, -0.8660254037844380415 ) ) ;
#5258=CARTESIAN_POINT ( 'NONE',  ( 4.000000000000003553, -3.518949890710769690, 0.000000000000000000 ) ) ;
#5259=UNCERTAINTY_MEASURE_WITH_UNIT (LENGTH_MEASURE( 1.000000000000000082E-05 ), #298, 'distance_accuracy_value', 'NONE');
#5261=CYLINDRICAL_SURFACE ( 'NONE', #6353, 4.000000000000030198 ) ;
#5293=LINE ( 'NONE', #4687, #7288 ) ;
#5299=CARTESIAN_POINT ( 'NONE',  ( 8.400000000000018119, -5.551115123125782702E-14, 6.661338147750939243E-13 ) ) ;
#5305=DIRECTION ( 'NONE',  ( 0.000000000000000000, 0.4999999999999986677, -0.8660254037844393737 ) ) ;
#5306=EDGE_CURVE ( 'NONE', #5464, #5847, #7186, .T. ) ;
#5308=FACE_OUTER_BOUND ( 'NONE', #7333, .T. ) ;
#5352=VERTEX_POINT ( 'NONE', #3379 ) ;
#5360=CARTESIAN_POINT ( 'NONE',  ( 0.000000000000000000, -1.759474945355374631, 3.047500000000091802 ) ) ;
#5369=DIRECTION ( 'NONE',  ( -1.000000000000000000, 3.549874073494553124E-30, 0.000000000000000000 ) ) ;
#5375=AXIS2_PLACEMENT_3D ( 'NONE', #909, #2863, #3475 ) ;
#5378=ORIENTED_EDGE ( 'NONE', *, *, #4213, .T. ) ;
#5403=EDGE_LOOP ( 'NONE', ( #5150, #7666 ) ) ;
#5407=CYLINDRICAL_SURFACE ( 'NONE', #5694, 4.000000000000030198 ) ;
#5419=CARTESIAN_POINT ( 'NONE',  ( 4.000000000000003553, 9.714451465470119729E-14, 0.000000000000000000 ) ) ;
#5421=( NAMED_UNIT ( * ) PLANE_ANGLE_UNIT ( ) SI_UNIT ( $, .RADIAN. ) );
#5423=AXIS2_PLACEMENT_3D ( 'NONE', #1338, #1857, #728 ) ;
#5436=FACE_OUTER_BOUND ( 'NONE', #4038, .T. ) ;
#5456=CARTESIAN_POINT ( 'NONE',  ( -31.74999999999994316, 0.000000000000000000, 0.000000000000000000 ) ) ;
#5461=FACE_OUTER_BOUND ( 'NONE', #4719, .T. ) ;
#5464=VERTEX_POINT ( 'NONE', #1002 ) ;
#5469=EDGE_CURVE ( 'NONE', #5857, #7532, #6323, .T. ) ;
#5490=CARTESIAN_POINT ( 'NONE',  ( 4.000000000000058620, 3.518949890710762585, 2.220446049250313081E-13 ) ) ;
#5502=CARTESIAN_POINT ( 'NONE',  ( 4.000000000000058620, 3.518949890710762585, 2.220446049250313081E-13 ) ) ;
#5519=DIRECTION ( 'NONE',  ( 0.000000000000000000, -1.042965139114318115E-29, 1.000000000000000000 ) ) ;
#5520=EDGE_CURVE ( 'NONE', #5835, #5464, #7339, .T. ) ;
#5522=ORIENTED_EDGE ( 'NONE', *, *, #4213, .F. ) ;
#5528=DIRECTION ( 'NONE',  ( 0.000000000000000000, -0.5000000000000009992, -0.8660254037844380415 ) ) ;
#5552=DIRECTION ( 'NONE',  ( -1.000000000000000000, 3.549874073494553124E-30, 0.000000000000000000 ) ) ;
#5575=CLOSED_SHELL ( 'NONE', ( #7913, #7326, #4247, #1301, #6560, #8390, #6703, #882, #8414, #3128, #4910, #4680, #6413, #7034, #3945, #1410, #7667, #4462, #1371, #2029, #5004, #824, #4515, #3641, #3080, #6127, #3107 ) ) ;
#5608=ORIENTED_EDGE ( 'NONE', *, *, #153, .T. ) ;
#5609=CARTESIAN_POINT ( 'NONE',  ( 8.000000000000014211, -5.497230663963304033E-14, 4.400000000000696687 ) ) ;
#5615=CARTESIAN_POINT ( 'NONE',  ( 8.400000000000018119, -5.551115123125777653E-14, -4.399999999999364420 ) ) ;
#5617=AXIS2_PLACEMENT_3D ( 'NONE', #4708, #2047, #3261 ) ;
#5629=AXIS2_PLACEMENT_3D ( 'NONE', #3018, #276, #5748 ) ;
#5639=CIRCLE ( 'NONE', #2842, 4.000000000000030198 ) ;
#5694=AXIS2_PLACEMENT_3D ( 'NONE', #5456, #7610, #834 ) ;
#5702=ORIENTED_EDGE ( 'NONE', *, *, #391, .T. ) ;
#5725=ORIENTED_EDGE ( 'NONE', *, *, #7377, .F. ) ;
#5737=VECTOR ( 'NONE', #5552, 1000.000000000000000 ) ;
#5748=DIRECTION ( 'NONE',  ( 0.000000000000000000, 1.224646799147288373E-16, 1.000000000000000000 ) ) ;
#5753=MANIFOLD_SOLID_BREP ( 'Hex', #5575 ) ;
#5774=EDGE_CURVE ( 'NONE', #698, #863, #2923, .T. ) ;
#5797=DIRECTION ( 'NONE',  ( -3.549874073494552424E-30, 0.5000000000000009992, 0.8660254037844380415 ) ) ;
#5801=ORIENTED_EDGE ( 'NONE', *, *, #5306, .T. ) ;
#5806=DIRECTION ( 'NONE',  ( 0.000000000000000000, -1.064348848528640685E-29, 1.000000000000000000 ) ) ;
#5835=VERTEX_POINT ( 'NONE', #1721 ) ;
#5837=DIRECTION ( 'NONE',  ( 0.000000000000000000, -1.213383262747659708E-29, 1.000000000000000000 ) ) ;
#5847=VERTEX_POINT ( 'NONE', #3074 ) ;
#5856=CARTESIAN_POINT ( 'NONE',  ( 4.000000000000003553, -3.518949890710769690, 0.000000000000000000 ) ) ;
#5857=VERTEX_POINT ( 'NONE', #3850 ) ;
#5858=DIRECTION ( 'NONE',  ( -1.000000000000000000, 3.549874073494553124E-30, 0.000000000000000000 ) ) ;
#5909=CARTESIAN_POINT ( 'NONE',  ( 0.7999999999999674039, 6.779273404243070203E-29, -6.499999999999968026 ) ) ;
#5913=DIRECTION ( 'NONE',  ( 3.549874073494553825E-30, -1.000000000000000000, 1.478898702612476446E-15 ) ) ;
#5931=DIRECTION ( 'NONE',  ( -1.000000000000000000, 3.549874073494553124E-30, 0.000000000000000000 ) ) ;
#5962=ORIENTED_EDGE ( 'NONE', *, *, #3824, .F. ) ;
#5966=DIRECTION ( 'NONE',  ( 0.7071067811865483499, 5.015942853700631228E-30, -0.7071067811865467956 ) ) ;
#5985=DIRECTION ( 'NONE',  ( -1.000000000000000000, 3.549874073494553124E-30, 3.778304382545602261E-59 ) ) ;
#5989=VECTOR ( 'NONE', #4474, 1000.000000000000227 ) ;
#6003=CIRCLE ( 'NONE', #7789, 3.047499999999999876 ) ;
#6022=DIRECTION ( 'NONE',  ( -1.000000000000000000, 3.549874073494553124E-30, 0.000000000000000000 ) ) ;
#6025=LINE ( 'NONE', #5360, #4176 ) ;
#6029=VECTOR ( 'NONE', #5931, 1000.000000000000000 ) ;
#6064=ORIENTED_EDGE ( 'NONE', *, *, #498, .T. ) ;
#6074=EDGE_CURVE ( 'NONE', #7841, #1496, #7997, .T. ) ;
#6077=CARTESIAN_POINT ( 'NONE',  ( 5.759474945355391284, 1.387778780781445676E-14, 0.000000000000000000 ) ) ;
#6088=EDGE_LOOP ( 'NONE', ( #1638, #3949, #6942 ) ) ;
#6092=EDGE_CURVE ( 'NONE', #4339, #5835, #1373, .T. ) ;
#6118=DIRECTION ( 'NONE',  ( 0.000000000000000000, -1.213383262747659708E-29, 1.000000000000000000 ) ) ;
#6123=CIRCLE ( 'NONE', #5423, 6.500000000000000888 ) ;
#6127=ADVANCED_FACE ( 'NONE', ( #1018 ), #3053, .T. ) ;
#6131=DIRECTION ( 'NONE',  ( -1.000000000000000000, 3.549874073494553124E-30, -0.000000000000000000 ) ) ;
#6170=ORIENTED_EDGE ( 'NONE', *, *, #7134, .F. ) ;
#6179=DIRECTION ( 'NONE',  ( -1.000000000000000000, 3.549874073494553124E-30, 0.000000000000000000 ) ) ;
#6184=VECTOR ( 'NONE', #6579, 1000.000000000000000 ) ;
#6190=CARTESIAN_POINT ( 'NONE',  ( 4.000000000000003553, -1.759474945355333109, 3.047500000000091802 ) ) ;
#6205=LINE ( 'NONE', #4834, #4648 ) ;
#6208=VERTEX_POINT ( 'NONE', #8371 ) ;
#6240=ORIENTED_EDGE ( 'NONE', *, *, #4995, .F. ) ;
#6276=DIRECTION ( 'NONE',  ( 3.549874073494553124E-30, -1.000000000000000000, 8.626909098572831859E-16 ) ) ;
#6279=FACE_OUTER_BOUND ( 'NONE', #4231, .T. ) ;
#6281=DIRECTION ( 'NONE',  ( 0.000000000000000000, 1.078520768856843950E-29, -1.000000000000000000 ) ) ;
#6304=CARTESIAN_POINT ( 'NONE',  ( 4.000000000000003553, -3.518949890710769690, 0.000000000000000000 ) ) ;
#6308=PLANE ( 'NONE',  #4577 ) ;
#6323=LINE ( 'NONE', #7658, #3129 ) ;
#6325=ORIENTED_EDGE ( 'NONE', *, *, #8332, .F. ) ;
#6353=AXIS2_PLACEMENT_3D ( 'NONE', #4747, #7961, #7912 ) ;
#6358=CARTESIAN_POINT ( 'NONE',  ( 4.000000000000003553, -3.518949890710769690, 0.000000000000000000 ) ) ;
#6399=LINE ( 'NONE', #471, #171 ) ;
#6401=DIRECTION ( 'NONE',  ( 0.000000000000000000, -1.064348848528640545E-29, 1.000000000000000000 ) ) ;
#6413=ADVANCED_FACE ( 'NONE', ( #7977 ), #3406, .T. ) ;
#6418=EDGE_LOOP ( 'NONE', ( #4416, #2125, #1305 ) ) ;
#6423=LINE ( 'NONE', #7683, #4871 ) ;
#6434=AXIS2_PLACEMENT_3D ( 'NONE', #1212, #5985, #654 ) ;
#6436=CARTESIAN_POINT ( 'NONE',  ( 32.30950000000065359, 0.000000000000000000, 6.883382752675970551E-12 ) ) ;
#6445=CARTESIAN_POINT ( 'NONE',  ( 0.000000000000000000, 0.000000000000000000, 0.000000000000000000 ) ) ;
#6448=EDGE_CURVE ( 'NONE', #173, #927, #22, .T. ) ;
#6450=ADVANCED_BREP_SHAPE_REPRESENTATION ( '', ( #5753, #7563 ), #4234 ) ;
#6456=CARTESIAN_POINT ( 'NONE',  ( 4.000000000000003553, 1.759474945355374409, 3.047499999999869758 ) ) ;
#6466=DIRECTION ( 'NONE',  ( -1.000000000000000000, 3.549874073494553124E-30, 0.000000000000000000 ) ) ;
#6499=CARTESIAN_POINT ( 'NONE',  ( 4.000000000000003553, -1.759474945355333109, 3.047500000000091802 ) ) ;
#6523=CIRCLE ( 'NONE', #693, 4.000000000000060396 ) ;
#6529=DIRECTION ( 'NONE',  ( 0.000000000000000000, -1.213383262747659708E-29, 1.000000000000000000 ) ) ;
#6533=CARTESIAN_POINT ( 'NONE',  ( 4.000000000000003553, -2.639212418033074936, 1.523750000000045901 ) ) ;
#6535=LINE ( 'NONE', #4672, #4334 ) ;
#6560=ADVANCED_FACE ( 'NONE', ( #2304 ), #301, .T. ) ;
#6573=AXIS2_PLACEMENT_3D ( 'NONE', #6456, #1264, #2483 ) ;
#6574=FACE_OUTER_BOUND ( 'NONE', #5403, .T. ) ;
#6579=DIRECTION ( 'NONE',  ( -3.549874073494553124E-30, 1.000000000000000000, -8.626909098572831859E-16 ) ) ;
#6586=AXIS2_PLACEMENT_3D ( 'NONE', #3540, #8029, #4841 ) ;
#6599=LINE ( 'NONE', #631, #1306 ) ;
#6611=DIRECTION ( 'NONE',  ( -5.620633949699709114E-30, 0.8660254037844393737, 0.4999999999999987232 ) ) ;
#6623=VERTEX_POINT ( 'NONE', #5502 ) ;
#6643=DIRECTION ( 'NONE',  ( 0.000000000000000000, 0.4999999999999983902, -0.8660254037844395958 ) ) ;
#6648=LINE ( 'NONE', #8596, #6957 ) ;
#6654=EDGE_LOOP ( 'NONE', ( #3312, #3459, #7302, #2783 ) ) ;
#6655=DIRECTION ( 'NONE',  ( 0.000000000000000000, -1.064348848528640545E-29, 1.000000000000000000 ) ) ;
#6703=ADVANCED_FACE ( 'NONE', ( #3045, #4566 ), #7058, .T. ) ;
#6709=ORIENTED_EDGE ( 'NONE', *, *, #856, .F. ) ;
#6710=FACE_OUTER_BOUND ( 'NONE', #1754, .T. ) ;
#6715=DIRECTION ( 'NONE',  ( 1.000000000000000000, -3.549874073494553124E-30, 0.000000000000000000 ) ) ;
#6716=CARTESIAN_POINT ( 'NONE',  ( 33.00000000000058265, 3.309499999999951481, 7.105427357601001859E-12 ) ) ;
#6719=CONICAL_SURFACE ( 'NONE', #2129, 3.047499999999999876, 1.047197551196592524 ) ;
#6733=ORIENTED_EDGE ( 'NONE', *, *, #7134, .T. ) ;
#6796=CARTESIAN_POINT ( 'NONE',  ( 4.000000000000058620, 3.518949890710762585, 2.220446049250313081E-13 ) ) ;
#6812=EDGE_CURVE ( 'NONE', #698, #5464, #1819, .T. ) ;
#6854=EDGE_CURVE ( 'NONE', #1642, #2701, #2081, .T. ) ;
#6858=VECTOR ( 'NONE', #1074, 1000.000000000000000 ) ;
#6859=LINE ( 'NONE', #2883, #5737 ) ;
#6863=VECTOR ( 'NONE', #7317, 1000.000000000000114 ) ;
#6865=ORIENTED_EDGE ( 'NONE', *, *, #7389, .F. ) ;
#6876=VERTEX_POINT ( 'NONE', #2781 ) ;
#6883=CARTESIAN_POINT ( 'NONE',  ( 0.000000000000000000, 0.000000000000000000, 0.000000000000000000 ) ) ;
#6890=CARTESIAN_POINT ( 'NONE',  ( 4.000000000000003553, 9.714451465470119729E-14, 0.000000000000000000 ) ) ;
#6895=ORIENTED_EDGE ( 'NONE', *, *, #2793, .T. ) ;
#6897=PLANE ( 'NONE',  #6586 ) ;
#6923=PLANE ( 'NONE',  #7461 ) ;
#6924=LINE ( 'NONE', #2903, #2529 ) ;
#6935=ORIENTED_EDGE ( 'NONE', *, *, #3774, .F. ) ;
#6942=ORIENTED_EDGE ( 'NONE', *, *, #498, .F. ) ;
#6951=DIRECTION ( 'NONE',  ( -1.000000000000000000, 3.549874073494553124E-30, 0.000000000000000000 ) ) ;
#6957=VECTOR ( 'NONE', #7951, 1000.000000000000000 ) ;
#6969=SHAPE_REPRESENTATION ( 'socket head cap screw_am_B18.3.1M - 8 x 1.25 x 25 Hex SHCS -- 25NHX', ( #7563 ), #4234 ) ;
#6976=( GEOMETRIC_REPRESENTATION_CONTEXT ( 3 ) GLOBAL_UNCERTAINTY_ASSIGNED_CONTEXT ( ( #5259 ) ) GLOBAL_UNIT_ASSIGNED_CONTEXT ( ( #298, #3447, #166 ) ) REPRESENTATION_CONTEXT ( 'NONE', 'WORKASPACE' ) );
#7008=CARTESIAN_POINT ( 'NONE',  ( 4.000000000000003553, -2.639212418033041185, -1.523750000000045901 ) ) ;
#7017=PRODUCT_DEFINITION ( 'UNKNOWN', '', #7297, #3240 ) ;
#7034=ADVANCED_FACE ( 'NONE', ( #6279 ), #4980, .F. ) ;
#7058=PLANE ( 'NONE',  #4575 ) ;
#7065=EDGE_CURVE ( 'NONE', #6623, #927, #1675, .T. ) ;
#7101=EDGE_LOOP ( 'NONE', ( #124, #7646, #954, #6064, #255 ) ) ;
#7103=ORIENTED_EDGE ( 'NONE', *, *, #5520, .F. ) ;
#7132=VECTOR ( 'NONE', #466, 1000.000000000000227 ) ;
#7134=EDGE_CURVE ( 'NONE', #5352, #3217, #7694, .T. ) ;
#7137=AXIS2_PLACEMENT_3D ( 'NONE', #3062, #4284, #7596 ) ;
#7159=PLANE ( 'NONE',  #7368 ) ;
#7167=UNCERTAINTY_MEASURE_WITH_UNIT (LENGTH_MEASURE( 1.000000000000000082E-05 ), #7330, 'distance_accuracy_value', 'NONE');
#7172=DIRECTION ( 'NONE',  ( 0.000000000000000000, -0.4999999999999983902, 0.8660254037844395958 ) ) ;
#7186=LINE ( 'NONE', #3828, #2224 ) ;
#7191=DIRECTION ( 'NONE',  ( -1.000000000000000000, 3.549874073494553124E-30, 0.000000000000000000 ) ) ;
#7202=SHAPE_REPRESENTATION_RELATIONSHIP ( 'NONE' , 'NONE' ,  #6969, #6450 ) ;
#7213=FACE_OUTER_BOUND ( 'NONE', #1088, .T. ) ;
#7217=EDGE_CURVE ( 'NONE', #3620, #1712, #6523, .T. ) ;
#7229=CIRCLE ( 'NONE', #1387, 4.400000000000030553 ) ;
#7239=AXIS2_PLACEMENT_3D ( 'NONE', #6890, #918, #251 ) ;
#7243=DIRECTION ( 'NONE',  ( -1.000000000000000000, 3.549874073494553124E-30, 0.000000000000000000 ) ) ;
#7259=DIRECTION ( 'NONE',  ( -1.000000000000000000, 3.549874073494553124E-30, 3.778304382545602261E-59 ) ) ;
#7278=CONICAL_SURFACE ( 'NONE', #1991, 5.700000000000001954, 0.7853981633974472798 ) ;
#7288=VECTOR ( 'NONE', #5247, 1000.000000000000000 ) ;
#7296=CARTESIAN_POINT ( 'NONE',  ( 32.30950000000065359, 4.898587196583831638E-16, -3.999999999993177457 ) ) ;
#7297=PRODUCT_DEFINITION_FORMATION_WITH_SPECIFIED_SOURCE ( 'ANY', '', #1179, .NOT_KNOWN. ) ;
#7302=ORIENTED_EDGE ( 'NONE', *, *, #2285, .T. ) ;
#7303=ORIENTED_EDGE ( 'NONE', *, *, #7735, .T. ) ;
#7311=EDGE_LOOP ( 'NONE', ( #1914, #1304, #1024 ) ) ;
#7317=DIRECTION ( 'NONE',  ( -0.7071067811864648611, 8.659560562356949384E-17, -0.7071067811866301733 ) ) ;
#7326=ADVANCED_FACE ( 'NONE', ( #5436 ), #7915, .F. ) ;
#7330=( LENGTH_UNIT ( ) NAMED_UNIT ( * ) SI_UNIT ( .MILLI., .METRE. ) );
#7333=EDGE_LOOP ( 'NONE', ( #2965, #8276, #240, #3429 ) ) ;
#7339=LINE ( 'NONE', #1196, #780 ) ;
#7368=AXIS2_PLACEMENT_3D ( 'NONE', #6499, #501, #5797 ) ;
#7375=ORIENTED_EDGE ( 'NONE', *, *, #2517, .T. ) ;
#7377=EDGE_CURVE ( 'NONE', #6208, #872, #3283, .T. ) ;
#7389=EDGE_CURVE ( 'NONE', #1496, #5847, #6648, .T. ) ;
#7391=LINE ( 'NONE', #6190, #733 ) ;
#7419=ORIENTED_EDGE ( 'NONE', *, *, #2285, .F. ) ;
#7453=VERTEX_POINT ( 'NONE', #2813 ) ;
#7461=AXIS2_PLACEMENT_3D ( 'NONE', #4166, #949, #6276 ) ;
#7478=DIRECTION ( 'NONE',  ( 0.000000000000000000, 0.000000000000000000, 1.000000000000000000 ) ) ;
#7500=EDGE_CURVE ( 'NONE', #4183, #896, #4030, .T. ) ;
#7532=VERTEX_POINT ( 'NONE', #8130 ) ;
#7563=AXIS2_PLACEMENT_3D ( 'NONE', #4203, #7478, #3512 ) ;
#7575=CARTESIAN_POINT ( 'NONE',  ( 32.30950000000065359, 0.000000000000000000, 6.883382752675970551E-12 ) ) ;
#7576=ORIENTED_EDGE ( 'NONE', *, *, #6854, .F. ) ;
#7596=DIRECTION ( 'NONE',  ( 0.000000000000000000, -1.213383262747659708E-29, 1.000000000000000000 ) ) ;
#7610=DIRECTION ( 'NONE',  ( -1.000000000000000000, 3.549874073494553124E-30, 0.000000000000000000 ) ) ;
#7628=DIRECTION ( 'NONE',  ( -1.000000000000000000, 3.549874073494553124E-30, 3.778304382545602261E-59 ) ) ;
#7646=ORIENTED_EDGE ( 'NONE', *, *, #1425, .F. ) ;
#7658=CARTESIAN_POINT ( 'NONE',  ( 4.000000000000003553, -1.759474945355333109, 3.047500000000091802 ) ) ;
#7666=ORIENTED_EDGE ( 'NONE', *, *, #7735, .F. ) ;
#7667=ADVANCED_FACE ( 'NONE', ( #8337 ), #7159, .T. ) ;
#7671=VECTOR ( 'NONE', #4825, 1000.000000000000000 ) ;
#7680=VECTOR ( 'NONE', #5369, 1000.000000000000000 ) ;
#7683=CARTESIAN_POINT ( 'NONE',  ( 4.000000000000003553, 1.759474945355374409, 3.047499999999869758 ) ) ;
#7694=LINE ( 'NONE', #5210, #5123 ) ;
#7697=LINE ( 'NONE', #1081, #2154 ) ;
#7713=DIRECTION ( 'NONE',  ( -0.7071067811864648611, -5.015942853701814625E-30, 0.7071067811866301733 ) ) ;
#7718=DIRECTION ( 'NONE',  ( 0.000000000000000000, -1.024214141749972931E-29, 1.000000000000000000 ) ) ;
#7735=EDGE_CURVE ( 'NONE', #1219, #7453, #273, .T. ) ;
#7744=DIRECTION ( 'NONE',  ( -1.000000000000000000, 3.549874073494553124E-30, 3.778304382545602261E-59 ) ) ;
#7752=CARTESIAN_POINT ( 'NONE',  ( 4.000000000000003553, 1.759474945355374409, 3.047499999999869758 ) ) ;
#7757=EDGE_CURVE ( 'NONE', #927, #5835, #6003, .T. ) ;
#7776=DIRECTION ( 'NONE',  ( 0.000000000000000000, 1.078520768856843950E-29, -1.000000000000000000 ) ) ;
#7787=MECHANICAL_DESIGN_GEOMETRIC_PRESENTATION_REPRESENTATION('',(#2791),#6976);
#7789=AXIS2_PLACEMENT_3D ( 'NONE', #2627, #3187, #7896 ) ;
#7807=VECTOR ( 'NONE', #4776, 1000.000000000000114 ) ;
#7838=PLANE ( 'NONE',  #3668 ) ;
#7841=VERTEX_POINT ( 'NONE', #5197 ) ;
#7877=AXIS2_PLACEMENT_3D ( 'NONE', #507, #8309, #4342 ) ;
#7882=FACE_OUTER_BOUND ( 'NONE', #1588, .T. ) ;
#7885=DIRECTION ( 'NONE',  ( 0.000000000000000000, -1.064348848528640545E-29, 1.000000000000000000 ) ) ;
#7890=CARTESIAN_POINT ( 'NONE',  ( 0.000000000000000000, -3.518949890710769690, 0.000000000000000000 ) ) ;
#7896=DIRECTION ( 'NONE',  ( 0.000000000000000000, -1.213383262747659708E-29, 1.000000000000000000 ) ) ;
#7901=DIRECTION ( 'NONE',  ( 5.620633949699709114E-30, -0.8660254037844395958, -0.4999999999999983902 ) ) ;
#7910=VECTOR ( 'NONE', #7713, 1000.000000000000114 ) ;
#7912=DIRECTION ( 'NONE',  ( 0.000000000000000000, -1.064348848528640685E-29, 1.000000000000000000 ) ) ;
#7913=ADVANCED_FACE ( 'NONE', ( #4931 ), #1943, .F. ) ;
#7915=TOROIDAL_SURFACE ( 'NONE', #8199, 4.400000000000030553, 0.4000000000000000222 ) ;
#7951=DIRECTION ( 'NONE',  ( 3.549874073494553825E-30, -1.000000000000000000, 1.478898702612476446E-15 ) ) ;
#7961=DIRECTION ( 'NONE',  ( -1.000000000000000000, 3.549874073494553124E-30, 0.000000000000000000 ) ) ;
#7966=VERTEX_POINT ( 'NONE', #2117 ) ;
#7977=FACE_OUTER_BOUND ( 'NONE', #2829, .T. ) ;
#7979=ORIENTED_EDGE ( 'NONE', *, *, #6448, .T. ) ;
#7997=LINE ( 'NONE', #1284, #6029 ) ;
#7998=DIRECTION ( 'NONE',  ( 1.000000000000000000, -3.549874073494553124E-30, 0.000000000000000000 ) ) ;
#8009=EDGE_CURVE ( 'NONE', #1219, #872, #6859, .T. ) ;
#8024=DIRECTION ( 'NONE',  ( -1.000000000000000000, 3.549874073494553124E-30, 0.000000000000000000 ) ) ;
#8029=DIRECTION ( 'NONE',  ( -1.000000000000000000, 3.549874073494553124E-30, 3.778304382545602261E-59 ) ) ;
#8035=ORIENTED_EDGE ( 'NONE', *, *, #6074, .F. ) ;
#8051=ORIENTED_EDGE ( 'NONE', *, *, #943, .F. ) ;
#8130=CARTESIAN_POINT ( 'NONE',  ( 4.000000000000003553, 6.938893903907228378E-14, 3.047499999999869758 ) ) ;
#8158=VERTEX_POINT ( 'NONE', #112 ) ;
#8174=ORIENTED_EDGE ( 'NONE', *, *, #177, .F. ) ;
#8199=AXIS2_PLACEMENT_3D ( 'NONE', #5299, #7998, #3426 ) ;
#8241=AXIS2_PLACEMENT_3D ( 'NONE', #5010, #7628, #403 ) ;
#8246=VECTOR ( 'NONE', #3113, 1000.000000000000114 ) ;
#8253=ORIENTED_EDGE ( 'NONE', *, *, #3793, .T. ) ;
#8264=FACE_OUTER_BOUND ( 'NONE', #7311, .T. ) ;
#8265=ORIENTED_EDGE ( 'NONE', *, *, #391, .F. ) ;
#8276=ORIENTED_EDGE ( 'NONE', *, *, #4048, .T. ) ;
#8283=EDGE_LOOP ( 'NONE', ( #6240, #2754, #1209, #971, #5801 ) ) ;
#8297=LINE ( 'NONE', #566, #6184 ) ;
#8309=DIRECTION ( 'NONE',  ( -1.000000000000000000, 3.549874073494553124E-30, 0.000000000000000000 ) ) ;
#8312=CARTESIAN_POINT ( 'NONE',  ( 8.400000000000018119, -5.551115123125782702E-14, 6.661338147750939243E-13 ) ) ;
#8315=DIRECTION ( 'NONE',  ( 0.000000000000000000, -1.064348848528640685E-29, 1.000000000000000000 ) ) ;
#8332=EDGE_CURVE ( 'NONE', #2938, #4183, #2060, .T. ) ;
#8337=FACE_OUTER_BOUND ( 'NONE', #1089, .T. ) ;
#8348=AXIS2_PLACEMENT_3D ( 'NONE', #8500, #7243, #5240 ) ;
#8369=DIRECTION ( 'NONE',  ( 0.000000000000000000, -1.024214141749972931E-29, 1.000000000000000000 ) ) ;
#8371=CARTESIAN_POINT ( 'NONE',  ( 2.254359249602142680E-58, 6.350533013084927146E-29, -5.700000000000001954 ) ) ;
#8372=CARTESIAN_POINT ( 'NONE',  ( 4.000000000000003553, 9.714451465470119729E-14, 0.000000000000000000 ) ) ;
#8387=DIRECTION ( 'NONE',  ( 0.000000000000000000, 1.953992523340276458E-14, -1.000000000000000000 ) ) ;
#8390=ADVANCED_FACE ( 'NONE', ( #4217 ), #3675, .T. ) ;
#8399=CARTESIAN_POINT ( 'NONE',  ( 8.400000000000018119, 9.010270651821244215E-27, 4.000000000000696332 ) ) ;
#8407=ORIENTED_EDGE ( 'NONE', *, *, #3461, .T. ) ;
#8414=ADVANCED_FACE ( 'NONE', ( #7213 ), #2463, .T. ) ;
#8423=SHAPE_DEFINITION_REPRESENTATION ( #8483, #6969 ) ;
#8425=ORIENTED_EDGE ( 'NONE', *, *, #866, .F. ) ;
#8432=AXIS2_PLACEMENT_3D ( 'NONE', #5155, #1040, #2507 ) ;
#8444=ORIENTED_EDGE ( 'NONE', *, *, #4196, .T. ) ;
#8456=EDGE_CURVE ( 'NONE', #6623, #173, #7697, .T. ) ;
#8464=ORIENTED_EDGE ( 'NONE', *, *, #6092, .F. ) ;
#8466=CARTESIAN_POINT ( 'NONE',  ( 33.00000000000055422, -1.386389088789023606E-14, -3.309499999993116504 ) ) ;
#8475=VECTOR ( 'NONE', #5966, 999.9999999999998863 ) ;
#8482=AXIS2_PLACEMENT_3D ( 'NONE', #7575, #3659, #8315 ) ;
#8483=PRODUCT_DEFINITION_SHAPE ( 'NONE', 'NONE',  #7017 ) ;
#8495=EDGE_LOOP ( 'NONE', ( #2134, #6170, #2414, #4287, #6865, #2014 ) ) ;
#8496=PLANE ( 'NONE',  #6573 ) ;
#8498=EDGE_CURVE ( 'NONE', #4183, #2938, #5639, .T. ) ;
#8500=CARTESIAN_POINT ( 'NONE',  ( 8.000000000000007105, 2.775557561562891351E-14, 6.661338147750939243E-13 ) ) ;
#8502=ORIENTED_EDGE ( 'NONE', *, *, #6092, .T. ) ;
#8509=CIRCLE ( 'NONE', #4078, 3.047499999999999876 ) ;
#8529=AXIS2_PLACEMENT_3D ( 'NONE', #5036, #4468, #6401 ) ;
#8530=PLANE ( 'NONE',  #5617 ) ;
#8540=ORIENTED_EDGE ( 'NONE', *, *, #5520, .T. ) ;
#8545=ORIENTED_EDGE ( 'NONE', *, *, #4162, .T. ) ;
#8574=DIRECTION ( 'NONE',  ( 0.000000000000000000, 1.064348848528640405E-29, -1.000000000000000000 ) ) ;
#8596=CARTESIAN_POINT ( 'NONE',  ( 0.000000000000000000, 1.759474945355512965, -3.047500000000091802 ) ) ;
#8664=COLOUR_RGB('Black',0.12,0.14,0.17);
#8665=FILL_AREA_STYLE_COLOUR('',#8664);
#8666=FILL_AREA_STYLE('',(#8665));
#8667=SURFACE_STYLE_FILL_AREA(#8666);
#8668=SURFACE_SIDE_STYLE('',(#8667));
#8669=SURFACE_STYLE_USAGE(.BOTH.,#8668);
#8670=PRESENTATION_STYLE_ASSIGNMENT((#8669));
ENDSEC;
END-ISO-10303-21;
